ISO-10303-21;
HEADER;
/* Generated by software containing ST-Developer
 * from STEP Tools, Inc. (www.steptools.com) 
 */

FILE_DESCRIPTION(
/* description */ ('Rack and pinion manual slide'),
/* implementation_level */ '2;1');

FILE_NAME(
/* name */ 'Flat Washer - M6.step',
/* time_stamp */ '2026-10-28T03:22:49-07:00',
/* author */ (''),
/* organization */ (''),
/* preprocessor_version */ 'ST-DEVELOPER v20.2',
/* originating_system */ 'Autodesk Translation Framework v15.17.0.0',
/* authorisation */ '');

FILE_SCHEMA (('AUTOMOTIVE_DESIGN { 1 0 10303 214 3 1 1 }'));
ENDSEC;

DATA;
#10=MECHANICAL_DESIGN_GEOMETRIC_PRESENTATION_REPRESENTATION('',(#782),#34851);
#683=SHAPE_REPRESENTATION_RELATIONSHIP('SRR','None',#35122,#729);
#729=ADVANCED_BREP_SHAPE_REPRESENTATION('',(#831),#34847);
#782=STYLED_ITEM('',(#35418),#831);
#831=MANIFOLD_SOLID_BREP('Body1',#13806);
#1039=FACE_BOUND('',#3197,.T.);
#1040=FACE_BOUND('',#3199,.T.);
#1520=PLANE('',#15541);
#1521=PLANE('',#15542);
#2249=FACE_OUTER_BOUND('',#3194,.T.);
#2250=FACE_OUTER_BOUND('',#3195,.T.);
#2251=FACE_OUTER_BOUND('',#3196,.T.);
#2252=FACE_OUTER_BOUND('',#3198,.T.);
#3194=EDGE_LOOP('',(#12756,#12757,#12758,#12759));
#3195=EDGE_LOOP('',(#12760,#12761,#12762,#12763));
#3196=EDGE_LOOP('',(#12764));
#3197=EDGE_LOOP('',(#12765));
#3198=EDGE_LOOP('',(#12766));
#3199=EDGE_LOOP('',(#12767));
#4487=LINE('',#34627,#5778);
#4488=LINE('',#34633,#5779);
#5778=VECTOR('',#19303,0.32);
#5779=VECTOR('',#19310,0.6);
#6208=CIRCLE('',#15536,0.32);
#6209=CIRCLE('',#15537,0.32);
#6210=CIRCLE('',#15539,0.6);
#6211=CIRCLE('',#15540,0.6);
#7401=VERTEX_POINT('',#34624);
#7402=VERTEX_POINT('',#34626);
#7403=VERTEX_POINT('',#34630);
#7404=VERTEX_POINT('',#34632);
#9190=EDGE_CURVE('',#7401,#7401,#6208,.T.);
#9191=EDGE_CURVE('',#7401,#7402,#4487,.T.);
#9192=EDGE_CURVE('',#7402,#7402,#6209,.T.);
#9193=EDGE_CURVE('',#7403,#7403,#6210,.T.);
#9194=EDGE_CURVE('',#7403,#7404,#4488,.T.);
#9195=EDGE_CURVE('',#7404,#7404,#6211,.T.);
#12756=ORIENTED_EDGE('',*,*,#9190,.F.);
#12757=ORIENTED_EDGE('',*,*,#9191,.T.);
#12758=ORIENTED_EDGE('',*,*,#9192,.T.);
#12759=ORIENTED_EDGE('',*,*,#9191,.F.);
#12760=ORIENTED_EDGE('',*,*,#9193,.F.);
#12761=ORIENTED_EDGE('',*,*,#9194,.T.);
#12762=ORIENTED_EDGE('',*,*,#9195,.T.);
#12763=ORIENTED_EDGE('',*,*,#9194,.F.);
#12764=ORIENTED_EDGE('',*,*,#9193,.T.);
#12765=ORIENTED_EDGE('',*,*,#9190,.T.);
#12766=ORIENTED_EDGE('',*,*,#9195,.F.);
#12767=ORIENTED_EDGE('',*,*,#9192,.F.);
#13007=CYLINDRICAL_SURFACE('',#15535,0.32);
#13008=CYLINDRICAL_SURFACE('',#15538,0.6);
#13727=ADVANCED_FACE('',(#2249),#13007,.F.);
#13728=ADVANCED_FACE('',(#2250),#13008,.T.);
#13729=ADVANCED_FACE('',(#2251,#1039),#1520,.T.);
#13730=ADVANCED_FACE('',(#2252,#1040),#1521,.F.);
#13806=CLOSED_SHELL('',(#13727,#13728,#13729,#13730));
#15534=AXIS2_PLACEMENT_3D('',#34622,#19297,#19298);
#15535=AXIS2_PLACEMENT_3D('',#34623,#19299,#19300);
#15536=AXIS2_PLACEMENT_3D('',#34625,#19301,#19302);
#15537=AXIS2_PLACEMENT_3D('',#34628,#19304,#19305);
#15538=AXIS2_PLACEMENT_3D('',#34629,#19306,#19307);
#15539=AXIS2_PLACEMENT_3D('',#34631,#19308,#19309);
#15540=AXIS2_PLACEMENT_3D('',#34634,#19311,#19312);
#15541=AXIS2_PLACEMENT_3D('',#34635,#19313,#19314);
#15542=AXIS2_PLACEMENT_3D('',#34636,#19315,#19316);
#19297=DIRECTION('axis',(0.,0.,1.));
#19298=DIRECTION('refdir',(1.,0.,0.));
#19299=DIRECTION('center_axis',(0.,1.,0.));
#19300=DIRECTION('ref_axis',(1.,0.,0.));
#19301=DIRECTION('center_axis',(0.,-1.,0.));
#19302=DIRECTION('ref_axis',(1.,0.,0.));
#19303=DIRECTION('',(0.,-1.,0.));
#19304=DIRECTION('center_axis',(0.,-1.,0.));
#19305=DIRECTION('ref_axis',(1.,0.,0.));
#19306=DIRECTION('center_axis',(0.,1.,0.));
#19307=DIRECTION('ref_axis',(1.,0.,0.));
#19308=DIRECTION('center_axis',(0.,1.,0.));
#19309=DIRECTION('ref_axis',(1.,0.,0.));
#19310=DIRECTION('',(0.,-1.,0.));
#19311=DIRECTION('center_axis',(0.,1.,0.));
#19312=DIRECTION('ref_axis',(1.,0.,0.));
#19313=DIRECTION('center_axis',(0.,1.,0.));
#19314=DIRECTION('ref_axis',(1.,0.,0.));
#19315=DIRECTION('center_axis',(0.,1.,0.));
#19316=DIRECTION('ref_axis',(1.,0.,0.));
#34622=CARTESIAN_POINT('',(0.,0.,0.));
#34623=CARTESIAN_POINT('Origin',(0.,0.,0.));
#34624=CARTESIAN_POINT('',(-0.32,0.16,3.91886975727153E-17));
#34625=CARTESIAN_POINT('Origin',(0.,0.16,0.));
#34626=CARTESIAN_POINT('',(-0.32,0.,3.91886975727153E-17));
#34627=CARTESIAN_POINT('',(-0.32,0.,3.91886975727153E-17));
#34628=CARTESIAN_POINT('Origin',(0.,0.,0.));
#34629=CARTESIAN_POINT('Origin',(0.,0.,0.));
#34630=CARTESIAN_POINT('',(-0.6,0.16,7.34788079488412E-17));
#34631=CARTESIAN_POINT('Origin',(0.,0.16,0.));
#34632=CARTESIAN_POINT('',(-0.6,0.,7.34788079488412E-17));
#34633=CARTESIAN_POINT('',(-0.6,0.,7.34788079488412E-17));
#34634=CARTESIAN_POINT('Origin',(0.,0.,0.));
#34635=CARTESIAN_POINT('Origin',(0.,0.16,0.));
#34636=CARTESIAN_POINT('Origin',(0.,0.,0.));
#34793=UNCERTAINTY_MEASURE_WITH_UNIT(LENGTH_MEASURE(0.001),#34852,
'DISTANCE_ACCURACY_VALUE',
'Maximum model space distance between geometric entities at asserted c
onnectivities');
#34797=UNCERTAINTY_MEASURE_WITH_UNIT(LENGTH_MEASURE(0.001),#34852,
'DISTANCE_ACCURACY_VALUE',
'Maximum model space distance between geometric entities at asserted c
onnectivities');
#34847=(
GEOMETRIC_REPRESENTATION_CONTEXT(3)
GLOBAL_UNCERTAINTY_ASSIGNED_CONTEXT((#34793))
GLOBAL_UNIT_ASSIGNED_CONTEXT((#34852,#34854,#34855))
REPRESENTATION_CONTEXT('','3D')
);
#34851=(
GEOMETRIC_REPRESENTATION_CONTEXT(3)
GLOBAL_UNCERTAINTY_ASSIGNED_CONTEXT((#34797))
GLOBAL_UNIT_ASSIGNED_CONTEXT((#34852,#34854,#34855))
REPRESENTATION_CONTEXT('','3D')
);
#34852=(
LENGTH_UNIT()
NAMED_UNIT(*)
SI_UNIT(.CENTI.,.METRE.)
);
#34854=(
NAMED_UNIT(*)
PLANE_ANGLE_UNIT()
SI_UNIT($,.RADIAN.)
);
#34855=(
NAMED_UNIT(*)
SI_UNIT($,.STERADIAN.)
SOLID_ANGLE_UNIT()
);
#34905=SHAPE_DEFINITION_REPRESENTATION(#35048,#35122);
#35048=PRODUCT_DEFINITION_SHAPE('',$,#35176);
#35122=SHAPE_REPRESENTATION('',(#15534),#34847);
#35126=PRODUCT_DEFINITION_CONTEXT('part definition',#35287,'design');
#35176=PRODUCT_DEFINITION('Flat Washer - M6','Flat Washer - M6',#35229,
#35126);
#35229=PRODUCT_DEFINITION_FORMATION('',$,#35338);
#35287=APPLICATION_CONTEXT(
'Core Data for Automotive Mechanical Design Process');
#35288=PRODUCT_CONTEXT('part definition',#35287,'mechanical');
#35338=PRODUCT('Flat Washer - M6','Flat Washer - M6','Flat Washer - M6',
(#35288));
#35412=COLOUR_RGB('Black',0.12,0.14,0.17);
#35413=FILL_AREA_STYLE_COLOUR('',#35412);
#35414=FILL_AREA_STYLE('',(#35413));
#35415=SURFACE_STYLE_FILL_AREA(#35414);
#35416=SURFACE_SIDE_STYLE('',(#35415));
#35417=SURFACE_STYLE_USAGE(.BOTH.,#35416);
#35418=PRESENTATION_STYLE_ASSIGNMENT((#35417));
ENDSEC;
END-ISO-10303-21;
